ISO-10303-21;
HEADER;
/* Generated by software containing ST-Developer
 * from STEP Tools, Inc. (www.steptools.com) 
 */

FILE_DESCRIPTION(
/* description */ ('PAT-082'),
/* implementation_level */ '2;1');

FILE_NAME(
/* name */ 'Mounting foot.step',
/* time_stamp */ '2026-10-29T20:16:13-07:00',
/* author */ (''),
/* organization */ (''),
/* preprocessor_version */ 'ST-DEVELOPER v20.2',
/* originating_system */ 'Autodesk Translation Framework v15.17.0.0',
/* authorisation */ '');

FILE_SCHEMA (('AUTOMOTIVE_DESIGN { 1 0 10303 214 3 1 1 }'));
ENDSEC;

DATA;
#10=MECHANICAL_DESIGN_GEOMETRIC_PRESENTATION_REPRESENTATION('',(#244),#8266);
#200=SHAPE_REPRESENTATION_RELATIONSHIP('SRR','None',#8362,#222);
#222=ADVANCED_BREP_SHAPE_REPRESENTATION('',(#266),#8246);
#244=STYLED_ITEM('',(#8530),#266);
#266=MANIFOLD_SOLID_BREP('Body1',#4584);
#294=FACE_BOUND('',#897,.T.);
#295=FACE_BOUND('',#898,.T.);
#296=FACE_BOUND('',#899,.T.);
#297=FACE_BOUND('',#900,.T.);
#298=FACE_BOUND('',#902,.T.);
#299=FACE_BOUND('',#903,.T.);
#300=FACE_BOUND('',#904,.T.);
#301=FACE_BOUND('',#905,.T.);
#427=PLANE('',#4900);
#428=PLANE('',#4905);
#429=PLANE('',#4924);
#430=PLANE('',#4925);
#431=PLANE('',#4926);
#432=PLANE('',#4927);
#433=PLANE('',#4928);
#434=PLANE('',#4929);
#602=FACE_OUTER_BOUND('',#884,.T.);
#603=FACE_OUTER_BOUND('',#885,.T.);
#604=FACE_OUTER_BOUND('',#886,.T.);
#605=FACE_OUTER_BOUND('',#887,.T.);
#606=FACE_OUTER_BOUND('',#888,.T.);
#607=FACE_OUTER_BOUND('',#889,.T.);
#608=FACE_OUTER_BOUND('',#890,.T.);
#609=FACE_OUTER_BOUND('',#891,.T.);
#610=FACE_OUTER_BOUND('',#892,.T.);
#611=FACE_OUTER_BOUND('',#893,.T.);
#612=FACE_OUTER_BOUND('',#894,.T.);
#613=FACE_OUTER_BOUND('',#895,.T.);
#614=FACE_OUTER_BOUND('',#896,.T.);
#615=FACE_OUTER_BOUND('',#901,.T.);
#884=EDGE_LOOP('',(#3206,#3207));
#885=EDGE_LOOP('',(#3208,#3209,#3210,#3211));
#886=EDGE_LOOP('',(#3212,#3213));
#887=EDGE_LOOP('',(#3214,#3215,#3216,#3217));
#888=EDGE_LOOP('',(#3218,#3219,#3220,#3221,#3222,#3223,#3224,#3225));
#889=EDGE_LOOP('',(#3226,#3227,#3228,#3229,#3230,#3231,#3232,#3233));
#890=EDGE_LOOP('',(#3234,#3235,#3236,#3237));
#891=EDGE_LOOP('',(#3238,#3239,#3240,#3241));
#892=EDGE_LOOP('',(#3242,#3243,#3244,#3245));
#893=EDGE_LOOP('',(#3246,#3247,#3248,#3249));
#894=EDGE_LOOP('',(#3250,#3251,#3252,#3253));
#895=EDGE_LOOP('',(#3254,#3255,#3256,#3257));
#896=EDGE_LOOP('',(#3258,#3259,#3260,#3261));
#897=EDGE_LOOP('',(#3262,#3263,#3264));
#898=EDGE_LOOP('',(#3265,#3266,#3267));
#899=EDGE_LOOP('',(#3268));
#900=EDGE_LOOP('',(#3269));
#901=EDGE_LOOP('',(#3270,#3271,#3272,#3273));
#902=EDGE_LOOP('',(#3274));
#903=EDGE_LOOP('',(#3275));
#904=EDGE_LOOP('',(#3276));
#905=EDGE_LOOP('',(#3277));
#1279=LINE('',#6945,#1634);
#1280=LINE('',#6948,#1635);
#1281=LINE('',#6956,#1636);
#1282=LINE('',#6959,#1637);
#1283=LINE('',#6964,#1638);
#1284=LINE('',#6971,#1639);
#1285=LINE('',#6978,#1640);
#1286=LINE('',#6984,#1641);
#1287=LINE('',#6989,#1642);
#1288=LINE('',#6991,#1643);
#1289=LINE('',#6993,#1644);
#1290=LINE('',#6994,#1645);
#1291=LINE('',#6997,#1646);
#1292=LINE('',#6999,#1647);
#1293=LINE('',#7000,#1648);
#1294=LINE('',#7003,#1649);
#1295=LINE('',#7005,#1650);
#1296=LINE('',#7006,#1651);
#1297=LINE('',#7008,#1652);
#1298=LINE('',#7009,#1653);
#1634=VECTOR('',#5536,1.);
#1635=VECTOR('',#5539,1.);
#1636=VECTOR('',#5548,1.);
#1637=VECTOR('',#5551,1.);
#1638=VECTOR('',#5556,0.275);
#1639=VECTOR('',#5565,0.275);
#1640=VECTOR('',#5574,0.275);
#1641=VECTOR('',#5581,0.275);
#1642=VECTOR('',#5586,1.);
#1643=VECTOR('',#5587,1.);
#1644=VECTOR('',#5588,1.);
#1645=VECTOR('',#5589,1.);
#1646=VECTOR('',#5592,1.);
#1647=VECTOR('',#5593,1.);
#1648=VECTOR('',#5594,1.);
#1649=VECTOR('',#5597,1.);
#1650=VECTOR('',#5598,1.);
#1651=VECTOR('',#5599,1.);
#1652=VECTOR('',#5602,1.);
#1653=VECTOR('',#5603,1.);
#1961=CIRCLE('',#4901,0.275);
#1962=CIRCLE('',#4902,0.45);
#1963=CIRCLE('',#4904,0.45);
#1964=CIRCLE('',#4906,0.275);
#1965=CIRCLE('',#4907,0.45);
#1966=CIRCLE('',#4909,0.45);
#1967=CIRCLE('',#4911,0.275);
#1968=CIRCLE('',#4912,0.275);
#1969=CIRCLE('',#4913,0.275);
#1970=CIRCLE('',#4915,0.275);
#1971=CIRCLE('',#4916,0.275);
#1972=CIRCLE('',#4917,0.275);
#1973=CIRCLE('',#4919,0.275);
#1974=CIRCLE('',#4920,0.275);
#1975=CIRCLE('',#4922,0.275);
#1976=CIRCLE('',#4923,0.275);
#2185=VERTEX_POINT('',#6939);
#2186=VERTEX_POINT('',#6940);
#2187=VERTEX_POINT('',#6944);
#2188=VERTEX_POINT('',#6946);
#2189=VERTEX_POINT('',#6950);
#2190=VERTEX_POINT('',#6951);
#2191=VERTEX_POINT('',#6955);
#2192=VERTEX_POINT('',#6957);
#2193=VERTEX_POINT('',#6961);
#2194=VERTEX_POINT('',#6963);
#2195=VERTEX_POINT('',#6968);
#2196=VERTEX_POINT('',#6970);
#2197=VERTEX_POINT('',#6975);
#2198=VERTEX_POINT('',#6977);
#2199=VERTEX_POINT('',#6981);
#2200=VERTEX_POINT('',#6983);
#2201=VERTEX_POINT('',#6987);
#2202=VERTEX_POINT('',#6988);
#2203=VERTEX_POINT('',#6990);
#2204=VERTEX_POINT('',#6992);
#2205=VERTEX_POINT('',#6996);
#2206=VERTEX_POINT('',#6998);
#2207=VERTEX_POINT('',#7002);
#2208=VERTEX_POINT('',#7004);
#2579=EDGE_CURVE('',#2185,#2186,#1961,.T.);
#2580=EDGE_CURVE('',#2185,#2186,#1962,.T.);
#2581=EDGE_CURVE('',#2187,#2185,#1279,.T.);
#2582=EDGE_CURVE('',#2188,#2187,#1963,.T.);
#2583=EDGE_CURVE('',#2186,#2188,#1280,.T.);
#2584=EDGE_CURVE('',#2189,#2190,#1964,.T.);
#2585=EDGE_CURVE('',#2189,#2190,#1965,.T.);
#2586=EDGE_CURVE('',#2191,#2189,#1281,.T.);
#2587=EDGE_CURVE('',#2192,#2191,#1966,.T.);
#2588=EDGE_CURVE('',#2190,#2192,#1282,.T.);
#2589=EDGE_CURVE('',#2193,#2193,#1967,.T.);
#2590=EDGE_CURVE('',#2193,#2194,#1283,.T.);
#2591=EDGE_CURVE('',#2187,#2194,#1968,.T.);
#2592=EDGE_CURVE('',#2194,#2188,#1969,.T.);
#2593=EDGE_CURVE('',#2195,#2195,#1970,.T.);
#2594=EDGE_CURVE('',#2195,#2196,#1284,.T.);
#2595=EDGE_CURVE('',#2191,#2196,#1971,.T.);
#2596=EDGE_CURVE('',#2196,#2192,#1972,.T.);
#2597=EDGE_CURVE('',#2197,#2197,#1973,.T.);
#2598=EDGE_CURVE('',#2197,#2198,#1285,.T.);
#2599=EDGE_CURVE('',#2198,#2198,#1974,.T.);
#2600=EDGE_CURVE('',#2199,#2199,#1975,.T.);
#2601=EDGE_CURVE('',#2199,#2200,#1286,.T.);
#2602=EDGE_CURVE('',#2200,#2200,#1976,.T.);
#2603=EDGE_CURVE('',#2201,#2202,#1287,.T.);
#2604=EDGE_CURVE('',#2202,#2203,#1288,.T.);
#2605=EDGE_CURVE('',#2204,#2203,#1289,.T.);
#2606=EDGE_CURVE('',#2201,#2204,#1290,.T.);
#2607=EDGE_CURVE('',#2205,#2201,#1291,.T.);
#2608=EDGE_CURVE('',#2206,#2204,#1292,.T.);
#2609=EDGE_CURVE('',#2205,#2206,#1293,.T.);
#2610=EDGE_CURVE('',#2207,#2205,#1294,.T.);
#2611=EDGE_CURVE('',#2208,#2206,#1295,.T.);
#2612=EDGE_CURVE('',#2207,#2208,#1296,.T.);
#2613=EDGE_CURVE('',#2202,#2207,#1297,.T.);
#2614=EDGE_CURVE('',#2203,#2208,#1298,.T.);
#3206=ORIENTED_EDGE('',*,*,#2579,.F.);
#3207=ORIENTED_EDGE('',*,*,#2580,.T.);
#3208=ORIENTED_EDGE('',*,*,#2581,.F.);
#3209=ORIENTED_EDGE('',*,*,#2582,.F.);
#3210=ORIENTED_EDGE('',*,*,#2583,.F.);
#3211=ORIENTED_EDGE('',*,*,#2580,.F.);
#3212=ORIENTED_EDGE('',*,*,#2584,.F.);
#3213=ORIENTED_EDGE('',*,*,#2585,.T.);
#3214=ORIENTED_EDGE('',*,*,#2586,.F.);
#3215=ORIENTED_EDGE('',*,*,#2587,.F.);
#3216=ORIENTED_EDGE('',*,*,#2588,.F.);
#3217=ORIENTED_EDGE('',*,*,#2585,.F.);
#3218=ORIENTED_EDGE('',*,*,#2589,.F.);
#3219=ORIENTED_EDGE('',*,*,#2590,.T.);
#3220=ORIENTED_EDGE('',*,*,#2591,.F.);
#3221=ORIENTED_EDGE('',*,*,#2581,.T.);
#3222=ORIENTED_EDGE('',*,*,#2579,.T.);
#3223=ORIENTED_EDGE('',*,*,#2583,.T.);
#3224=ORIENTED_EDGE('',*,*,#2592,.F.);
#3225=ORIENTED_EDGE('',*,*,#2590,.F.);
#3226=ORIENTED_EDGE('',*,*,#2593,.F.);
#3227=ORIENTED_EDGE('',*,*,#2594,.T.);
#3228=ORIENTED_EDGE('',*,*,#2595,.F.);
#3229=ORIENTED_EDGE('',*,*,#2586,.T.);
#3230=ORIENTED_EDGE('',*,*,#2584,.T.);
#3231=ORIENTED_EDGE('',*,*,#2588,.T.);
#3232=ORIENTED_EDGE('',*,*,#2596,.F.);
#3233=ORIENTED_EDGE('',*,*,#2594,.F.);
#3234=ORIENTED_EDGE('',*,*,#2597,.F.);
#3235=ORIENTED_EDGE('',*,*,#2598,.T.);
#3236=ORIENTED_EDGE('',*,*,#2599,.F.);
#3237=ORIENTED_EDGE('',*,*,#2598,.F.);
#3238=ORIENTED_EDGE('',*,*,#2600,.F.);
#3239=ORIENTED_EDGE('',*,*,#2601,.T.);
#3240=ORIENTED_EDGE('',*,*,#2602,.F.);
#3241=ORIENTED_EDGE('',*,*,#2601,.F.);
#3242=ORIENTED_EDGE('',*,*,#2603,.T.);
#3243=ORIENTED_EDGE('',*,*,#2604,.T.);
#3244=ORIENTED_EDGE('',*,*,#2605,.F.);
#3245=ORIENTED_EDGE('',*,*,#2606,.F.);
#3246=ORIENTED_EDGE('',*,*,#2607,.T.);
#3247=ORIENTED_EDGE('',*,*,#2606,.T.);
#3248=ORIENTED_EDGE('',*,*,#2608,.F.);
#3249=ORIENTED_EDGE('',*,*,#2609,.F.);
#3250=ORIENTED_EDGE('',*,*,#2610,.T.);
#3251=ORIENTED_EDGE('',*,*,#2609,.T.);
#3252=ORIENTED_EDGE('',*,*,#2611,.F.);
#3253=ORIENTED_EDGE('',*,*,#2612,.F.);
#3254=ORIENTED_EDGE('',*,*,#2613,.T.);
#3255=ORIENTED_EDGE('',*,*,#2612,.T.);
#3256=ORIENTED_EDGE('',*,*,#2614,.F.);
#3257=ORIENTED_EDGE('',*,*,#2604,.F.);
#3258=ORIENTED_EDGE('',*,*,#2614,.T.);
#3259=ORIENTED_EDGE('',*,*,#2611,.T.);
#3260=ORIENTED_EDGE('',*,*,#2608,.T.);
#3261=ORIENTED_EDGE('',*,*,#2605,.T.);
#3262=ORIENTED_EDGE('',*,*,#2582,.T.);
#3263=ORIENTED_EDGE('',*,*,#2591,.T.);
#3264=ORIENTED_EDGE('',*,*,#2592,.T.);
#3265=ORIENTED_EDGE('',*,*,#2587,.T.);
#3266=ORIENTED_EDGE('',*,*,#2595,.T.);
#3267=ORIENTED_EDGE('',*,*,#2596,.T.);
#3268=ORIENTED_EDGE('',*,*,#2599,.T.);
#3269=ORIENTED_EDGE('',*,*,#2602,.T.);
#3270=ORIENTED_EDGE('',*,*,#2613,.F.);
#3271=ORIENTED_EDGE('',*,*,#2603,.F.);
#3272=ORIENTED_EDGE('',*,*,#2607,.F.);
#3273=ORIENTED_EDGE('',*,*,#2610,.F.);
#3274=ORIENTED_EDGE('',*,*,#2589,.T.);
#3275=ORIENTED_EDGE('',*,*,#2597,.T.);
#3276=ORIENTED_EDGE('',*,*,#2600,.T.);
#3277=ORIENTED_EDGE('',*,*,#2593,.T.);
#4228=CYLINDRICAL_SURFACE('',#4903,0.45);
#4229=CYLINDRICAL_SURFACE('',#4908,0.45);
#4230=CYLINDRICAL_SURFACE('',#4910,0.275);
#4231=CYLINDRICAL_SURFACE('',#4914,0.275);
#4232=CYLINDRICAL_SURFACE('',#4918,0.275);
#4233=CYLINDRICAL_SURFACE('',#4921,0.275);
#4341=ADVANCED_FACE('',(#602),#427,.T.);
#4342=ADVANCED_FACE('',(#603),#4228,.F.);
#4343=ADVANCED_FACE('',(#604),#428,.T.);
#4344=ADVANCED_FACE('',(#605),#4229,.F.);
#4345=ADVANCED_FACE('',(#606),#4230,.F.);
#4346=ADVANCED_FACE('',(#607),#4231,.F.);
#4347=ADVANCED_FACE('',(#608),#4232,.F.);
#4348=ADVANCED_FACE('',(#609),#4233,.F.);
#4349=ADVANCED_FACE('',(#610),#429,.T.);
#4350=ADVANCED_FACE('',(#611),#430,.T.);
#4351=ADVANCED_FACE('',(#612),#431,.T.);
#4352=ADVANCED_FACE('',(#613),#432,.T.);
#4353=ADVANCED_FACE('',(#614,#294,#295,#296,#297),#433,.T.);
#4354=ADVANCED_FACE('',(#615,#298,#299,#300,#301),#434,.F.);
#4584=CLOSED_SHELL('',(#4341,#4342,#4343,#4344,#4345,#4346,#4347,#4348,
#4349,#4350,#4351,#4352,#4353,#4354));
#4899=AXIS2_PLACEMENT_3D('',#6937,#5526,#5527);
#4900=AXIS2_PLACEMENT_3D('',#6938,#5528,#5529);
#4901=AXIS2_PLACEMENT_3D('',#6941,#5530,#5531);
#4902=AXIS2_PLACEMENT_3D('',#6942,#5532,#5533);
#4903=AXIS2_PLACEMENT_3D('',#6943,#5534,#5535);
#4904=AXIS2_PLACEMENT_3D('',#6947,#5537,#5538);
#4905=AXIS2_PLACEMENT_3D('',#6949,#5540,#5541);
#4906=AXIS2_PLACEMENT_3D('',#6952,#5542,#5543);
#4907=AXIS2_PLACEMENT_3D('',#6953,#5544,#5545);
#4908=AXIS2_PLACEMENT_3D('',#6954,#5546,#5547);
#4909=AXIS2_PLACEMENT_3D('',#6958,#5549,#5550);
#4910=AXIS2_PLACEMENT_3D('',#6960,#5552,#5553);
#4911=AXIS2_PLACEMENT_3D('',#6962,#5554,#5555);
#4912=AXIS2_PLACEMENT_3D('',#6965,#5557,#5558);
#4913=AXIS2_PLACEMENT_3D('',#6966,#5559,#5560);
#4914=AXIS2_PLACEMENT_3D('',#6967,#5561,#5562);
#4915=AXIS2_PLACEMENT_3D('',#6969,#5563,#5564);
#4916=AXIS2_PLACEMENT_3D('',#6972,#5566,#5567);
#4917=AXIS2_PLACEMENT_3D('',#6973,#5568,#5569);
#4918=AXIS2_PLACEMENT_3D('',#6974,#5570,#5571);
#4919=AXIS2_PLACEMENT_3D('',#6976,#5572,#5573);
#4920=AXIS2_PLACEMENT_3D('',#6979,#5575,#5576);
#4921=AXIS2_PLACEMENT_3D('',#6980,#5577,#5578);
#4922=AXIS2_PLACEMENT_3D('',#6982,#5579,#5580);
#4923=AXIS2_PLACEMENT_3D('',#6985,#5582,#5583);
#4924=AXIS2_PLACEMENT_3D('',#6986,#5584,#5585);
#4925=AXIS2_PLACEMENT_3D('',#6995,#5590,#5591);
#4926=AXIS2_PLACEMENT_3D('',#7001,#5595,#5596);
#4927=AXIS2_PLACEMENT_3D('',#7007,#5600,#5601);
#4928=AXIS2_PLACEMENT_3D('',#7010,#5604,#5605);
#4929=AXIS2_PLACEMENT_3D('',#7011,#5606,#5607);
#5526=DIRECTION('axis',(0.,0.,1.));
#5527=DIRECTION('refdir',(1.,0.,0.));
#5528=DIRECTION('center_axis',(0.,0.,1.));
#5529=DIRECTION('ref_axis',(1.,0.,0.));
#5530=DIRECTION('center_axis',(0.,0.,1.));
#5531=DIRECTION('ref_axis',(1.,0.,0.));
#5532=DIRECTION('center_axis',(0.,0.,1.));
#5533=DIRECTION('ref_axis',(1.,0.,0.));
#5534=DIRECTION('center_axis',(0.,0.,1.));
#5535=DIRECTION('ref_axis',(0.78086880944303,0.624695047554425,0.));
#5536=DIRECTION('',(0.,0.,-1.));
#5537=DIRECTION('center_axis',(0.,0.,-1.));
#5538=DIRECTION('ref_axis',(1.,0.,0.));
#5539=DIRECTION('',(0.,0.,1.));
#5540=DIRECTION('center_axis',(0.,0.,1.));
#5541=DIRECTION('ref_axis',(1.,0.,0.));
#5542=DIRECTION('center_axis',(0.,0.,1.));
#5543=DIRECTION('ref_axis',(1.,0.,0.));
#5544=DIRECTION('center_axis',(0.,0.,1.));
#5545=DIRECTION('ref_axis',(1.,0.,0.));
#5546=DIRECTION('center_axis',(0.,0.,1.));
#5547=DIRECTION('ref_axis',(0.78086880944303,-0.624695047554425,0.));
#5548=DIRECTION('',(0.,0.,-1.));
#5549=DIRECTION('center_axis',(0.,0.,-1.));
#5550=DIRECTION('ref_axis',(1.,0.,0.));
#5551=DIRECTION('',(0.,0.,1.));
#5552=DIRECTION('center_axis',(0.,0.,1.));
#5553=DIRECTION('ref_axis',(1.,0.,0.));
#5554=DIRECTION('center_axis',(0.,0.,1.));
#5555=DIRECTION('ref_axis',(1.,0.,0.));
#5556=DIRECTION('',(0.,0.,1.));
#5557=DIRECTION('center_axis',(0.,0.,-1.));
#5558=DIRECTION('ref_axis',(1.,0.,0.));
#5559=DIRECTION('center_axis',(0.,0.,-1.));
#5560=DIRECTION('ref_axis',(1.,0.,0.));
#5561=DIRECTION('center_axis',(0.,0.,1.));
#5562=DIRECTION('ref_axis',(1.,0.,0.));
#5563=DIRECTION('center_axis',(0.,0.,1.));
#5564=DIRECTION('ref_axis',(1.,0.,0.));
#5565=DIRECTION('',(0.,0.,1.));
#5566=DIRECTION('center_axis',(0.,0.,-1.));
#5567=DIRECTION('ref_axis',(1.,0.,0.));
#5568=DIRECTION('center_axis',(0.,0.,-1.));
#5569=DIRECTION('ref_axis',(1.,0.,0.));
#5570=DIRECTION('center_axis',(0.,0.,1.));
#5571=DIRECTION('ref_axis',(1.,0.,0.));
#5572=DIRECTION('center_axis',(0.,0.,1.));
#5573=DIRECTION('ref_axis',(1.,0.,0.));
#5574=DIRECTION('',(0.,0.,1.));
#5575=DIRECTION('center_axis',(0.,0.,-1.));
#5576=DIRECTION('ref_axis',(1.,0.,0.));
#5577=DIRECTION('center_axis',(0.,0.,1.));
#5578=DIRECTION('ref_axis',(1.,0.,0.));
#5579=DIRECTION('center_axis',(0.,0.,1.));
#5580=DIRECTION('ref_axis',(1.,0.,0.));
#5581=DIRECTION('',(0.,0.,1.));
#5582=DIRECTION('center_axis',(0.,0.,-1.));
#5583=DIRECTION('ref_axis',(1.,0.,0.));
#5584=DIRECTION('center_axis',(0.,1.,0.));
#5585=DIRECTION('ref_axis',(-1.,0.,0.));
#5586=DIRECTION('',(-1.,0.,0.));
#5587=DIRECTION('',(0.,0.,1.));
#5588=DIRECTION('',(-1.,0.,0.));
#5589=DIRECTION('',(0.,0.,1.));
#5590=DIRECTION('center_axis',(1.,0.,0.));
#5591=DIRECTION('ref_axis',(0.,1.,0.));
#5592=DIRECTION('',(0.,1.,0.));
#5593=DIRECTION('',(0.,1.,0.));
#5594=DIRECTION('',(0.,0.,1.));
#5595=DIRECTION('center_axis',(0.,-1.,0.));
#5596=DIRECTION('ref_axis',(1.,0.,0.));
#5597=DIRECTION('',(1.,0.,0.));
#5598=DIRECTION('',(1.,0.,0.));
#5599=DIRECTION('',(0.,0.,1.));
#5600=DIRECTION('center_axis',(-1.,0.,0.));
#5601=DIRECTION('ref_axis',(0.,-1.,0.));
#5602=DIRECTION('',(0.,-1.,0.));
#5603=DIRECTION('',(0.,-1.,0.));
#5604=DIRECTION('center_axis',(0.,0.,1.));
#5605=DIRECTION('ref_axis',(1.,0.,0.));
#5606=DIRECTION('center_axis',(0.,0.,1.));
#5607=DIRECTION('ref_axis',(1.,0.,0.));
#6937=CARTESIAN_POINT('',(0.,0.,0.));
#6938=CARTESIAN_POINT('Origin',(-4.5,-1.4,0.9));
#6939=CARTESIAN_POINT('',(-4.72519681057161,-1.78959773678549,0.9));
#6940=CARTESIAN_POINT('',(-4.92952879918449,-1.53418275101939,0.9));
#6941=CARTESIAN_POINT('Origin',(-5.,-1.8,0.9));
#6942=CARTESIAN_POINT('Origin',(-4.5,-1.4,0.9));
#6943=CARTESIAN_POINT('Origin',(-4.5,-1.4,0.9));
#6944=CARTESIAN_POINT('',(-4.72519681057161,-1.78959773678549,1.4));
#6945=CARTESIAN_POINT('',(-4.72519681057161,-1.78959773678549,0.9));
#6946=CARTESIAN_POINT('',(-4.92952879918449,-1.53418275101939,1.4));
#6947=CARTESIAN_POINT('Origin',(-4.5,-1.4,1.4));
#6948=CARTESIAN_POINT('',(-4.92952879918449,-1.53418275101939,0.9));
#6949=CARTESIAN_POINT('Origin',(-4.5,1.4,0.9));
#6950=CARTESIAN_POINT('',(-4.92952879918449,1.53418275101939,0.9));
#6951=CARTESIAN_POINT('',(-4.72519681057161,1.78959773678549,0.9));
#6952=CARTESIAN_POINT('Origin',(-5.,1.8,0.9));
#6953=CARTESIAN_POINT('Origin',(-4.5,1.4,0.9));
#6954=CARTESIAN_POINT('Origin',(-4.5,1.4,0.9));
#6955=CARTESIAN_POINT('',(-4.92952879918449,1.53418275101939,1.4));
#6956=CARTESIAN_POINT('',(-4.92952879918449,1.53418275101939,0.9));
#6957=CARTESIAN_POINT('',(-4.72519681057161,1.78959773678549,1.4));
#6958=CARTESIAN_POINT('Origin',(-4.5,1.4,1.4));
#6959=CARTESIAN_POINT('',(-4.72519681057161,1.78959773678549,0.9));
#6960=CARTESIAN_POINT('Origin',(-5.,-1.8,0.3));
#6961=CARTESIAN_POINT('',(-5.275,-1.8,0.4));
#6962=CARTESIAN_POINT('Origin',(-5.,-1.8,0.4));
#6963=CARTESIAN_POINT('',(-5.275,-1.8,1.4));
#6964=CARTESIAN_POINT('',(-5.275,-1.8,0.3));
#6965=CARTESIAN_POINT('Origin',(-5.,-1.8,1.4));
#6966=CARTESIAN_POINT('Origin',(-5.,-1.8,1.4));
#6967=CARTESIAN_POINT('Origin',(-5.,1.8,0.3));
#6968=CARTESIAN_POINT('',(-5.275,1.8,0.4));
#6969=CARTESIAN_POINT('Origin',(-5.,1.8,0.4));
#6970=CARTESIAN_POINT('',(-5.275,1.8,1.4));
#6971=CARTESIAN_POINT('',(-5.275,1.8,0.3));
#6972=CARTESIAN_POINT('Origin',(-5.,1.8,1.4));
#6973=CARTESIAN_POINT('Origin',(-5.,1.8,1.4));
#6974=CARTESIAN_POINT('Origin',(-5.,2.8,0.3));
#6975=CARTESIAN_POINT('',(-5.275,2.8,0.4));
#6976=CARTESIAN_POINT('Origin',(-5.,2.8,0.4));
#6977=CARTESIAN_POINT('',(-5.275,2.8,1.4));
#6978=CARTESIAN_POINT('',(-5.275,2.8,0.3));
#6979=CARTESIAN_POINT('Origin',(-5.,2.8,1.4));
#6980=CARTESIAN_POINT('Origin',(-5.,-2.8,0.3));
#6981=CARTESIAN_POINT('',(-5.275,-2.8,0.4));
#6982=CARTESIAN_POINT('Origin',(-5.,-2.8,0.4));
#6983=CARTESIAN_POINT('',(-5.275,-2.8,1.4));
#6984=CARTESIAN_POINT('',(-5.275,-2.8,0.3));
#6985=CARTESIAN_POINT('Origin',(-5.,-2.8,1.4));
#6986=CARTESIAN_POINT('Origin',(-4.,3.6,0.4));
#6987=CARTESIAN_POINT('',(-4.,3.6,0.4));
#6988=CARTESIAN_POINT('',(-6.,3.6,0.4));
#6989=CARTESIAN_POINT('',(-4.,3.6,0.4));
#6990=CARTESIAN_POINT('',(-6.,3.6,1.4));
#6991=CARTESIAN_POINT('',(-6.,3.6,0.4));
#6992=CARTESIAN_POINT('',(-4.,3.6,1.4));
#6993=CARTESIAN_POINT('',(-4.,3.6,1.4));
#6994=CARTESIAN_POINT('',(-4.,3.6,0.4));
#6995=CARTESIAN_POINT('Origin',(-4.,-3.6,0.4));
#6996=CARTESIAN_POINT('',(-4.,-3.6,0.4));
#6997=CARTESIAN_POINT('',(-4.,-3.6,0.4));
#6998=CARTESIAN_POINT('',(-4.,-3.6,1.4));
#6999=CARTESIAN_POINT('',(-4.,-3.6,1.4));
#7000=CARTESIAN_POINT('',(-4.,-3.6,0.4));
#7001=CARTESIAN_POINT('Origin',(-6.,-3.6,0.4));
#7002=CARTESIAN_POINT('',(-6.,-3.6,0.4));
#7003=CARTESIAN_POINT('',(-6.,-3.6,0.4));
#7004=CARTESIAN_POINT('',(-6.,-3.6,1.4));
#7005=CARTESIAN_POINT('',(-6.,-3.6,1.4));
#7006=CARTESIAN_POINT('',(-6.,-3.6,0.4));
#7007=CARTESIAN_POINT('Origin',(-6.,3.6,0.4));
#7008=CARTESIAN_POINT('',(-6.,3.6,0.4));
#7009=CARTESIAN_POINT('',(-6.,3.6,1.4));
#7010=CARTESIAN_POINT('Origin',(-5.,0.,1.4));
#7011=CARTESIAN_POINT('Origin',(-5.,0.,0.4));
#8221=UNCERTAINTY_MEASURE_WITH_UNIT(LENGTH_MEASURE(0.001),#8267,
'DISTANCE_ACCURACY_VALUE',
'Maximum model space distance between geometric entities at asserted c
onnectivities');
#8241=UNCERTAINTY_MEASURE_WITH_UNIT(LENGTH_MEASURE(0.001),#8267,
'DISTANCE_ACCURACY_VALUE',
'Maximum model space distance between geometric entities at asserted c
onnectivities');
#8246=(
GEOMETRIC_REPRESENTATION_CONTEXT(3)
GLOBAL_UNCERTAINTY_ASSIGNED_CONTEXT((#8221))
GLOBAL_UNIT_ASSIGNED_CONTEXT((#8267,#8269,#8270))
REPRESENTATION_CONTEXT('','3D')
);
#8266=(
GEOMETRIC_REPRESENTATION_CONTEXT(3)
GLOBAL_UNCERTAINTY_ASSIGNED_CONTEXT((#8241))
GLOBAL_UNIT_ASSIGNED_CONTEXT((#8267,#8269,#8270))
REPRESENTATION_CONTEXT('','3D')
);
#8267=(
LENGTH_UNIT()
NAMED_UNIT(*)
SI_UNIT(.CENTI.,.METRE.)
);
#8269=(
NAMED_UNIT(*)
PLANE_ANGLE_UNIT()
SI_UNIT($,.RADIAN.)
);
#8270=(
NAMED_UNIT(*)
SI_UNIT($,.STERADIAN.)
SOLID_ANGLE_UNIT()
);
#8275=SHAPE_DEFINITION_REPRESENTATION(#8299,#8362);
#8299=PRODUCT_DEFINITION_SHAPE('',$,#8387);
#8362=SHAPE_REPRESENTATION('',(#4899),#8246);
#8382=PRODUCT_DEFINITION_CONTEXT('part definition',#8456,'design');
#8387=PRODUCT_DEFINITION('Mounting foot','Mounting foot',#8411,
#8382);
#8411=PRODUCT_DEFINITION_FORMATION('',$,#8462);
#8456=APPLICATION_CONTEXT(
'Core Data for Automotive Mechanical Design Process');
#8457=PRODUCT_CONTEXT('part definition',#8456,'mechanical');
#8462=PRODUCT('Mounting foot','Mounting foot',
'Mounting foot',(#8457));
#8524=COLOUR_RGB('Sky Blue',0.24,0.69,0.87);
#8525=FILL_AREA_STYLE_COLOUR('',#8524);
#8526=FILL_AREA_STYLE('',(#8525));
#8527=SURFACE_STYLE_FILL_AREA(#8526);
#8528=SURFACE_SIDE_STYLE('',(#8527));
#8529=SURFACE_STYLE_USAGE(.BOTH.,#8528);
#8530=PRESENTATION_STYLE_ASSIGNMENT((#8529));
ENDSEC;
END-ISO-10303-21;
